ISO-10303-21;
HEADER;
/* Generated by software containing ST-Developer
 * from STEP Tools, Inc. (www.steptools.com) 
 */
/* OPTION: using custom renumber hook */

FILE_DESCRIPTION(
/* description */ ('STEP AP242 Edition 2', 'CAx-IF Rec.Pracs.---Representation and Presentation of Product Manufa
cturing Information (PMI)---4.0---2014-10-13', 'CAx-IF Rec.Pracs.---3D Tessellated Geometry---0.4---2014-09-14', '2;1', 'CAx-IF Rec.Pracs.---User Defined Attributes---1.5---2016-08-15'),
/* implementation_level */ '2;1');

FILE_NAME(
/* name */ 'Part 2.step',
/* time_stamp */ '2026-10-07T00:00:55Z',
/* author */ (''),
/* organization */ (''),
/* preprocessor_version */ 'ST-DEVELOPER v20',
/* originating_system */ 'ONSHAPE BY PTC INC, 1.221',
/* authorisation */ '  ');

FILE_SCHEMA (('AP242_MANAGED_MODEL_BASED_3D_ENGINEERING_MIM_LF { 1 0 10303 442 3 1 4 }'));
ENDSEC;

DATA;
#41=ELLIPSE('',#4605,0.00141421356237309,0.001);
#42=ELLIPSE('',#4607,0.00141421356237309,0.001);
#43=ELLIPSE('',#4609,0.00141421356237309,0.001);
#44=ELLIPSE('',#4611,0.00141421356237309,0.001);
#122=SHAPE_REPRESENTATION_RELATIONSHIP('','',#4478,#133);
#133=ADVANCED_BREP_SHAPE_REPRESENTATION('',(#4454),#8541);
#140=TOROIDAL_SURFACE('',#4600,0.03,0.001);
#141=TOROIDAL_SURFACE('',#4602,0.03,0.001);
#142=TOROIDAL_SURFACE('',#4620,0.027,0.001);
#143=TOROIDAL_SURFACE('',#4624,0.027,0.001);
#225=CYLINDRICAL_SURFACE('',#4597,0.031);
#226=CYLINDRICAL_SURFACE('',#4604,0.001);
#227=CYLINDRICAL_SURFACE('',#4606,0.001);
#228=CYLINDRICAL_SURFACE('',#4608,0.001);
#229=CYLINDRICAL_SURFACE('',#4610,0.001);
#230=CYLINDRICAL_SURFACE('',#4612,0.001);
#231=CYLINDRICAL_SURFACE('',#4614,0.001);
#232=CYLINDRICAL_SURFACE('',#4623,0.026);
#233=CYLINDRICAL_SURFACE('',#4630,0.026);
#234=CYLINDRICAL_SURFACE('',#4631,0.024);
#235=CYLINDRICAL_SURFACE('',#4632,0.001);
#236=CYLINDRICAL_SURFACE('',#4634,0.001);
#237=CYLINDRICAL_SURFACE('',#4641,0.0045);
#238=CYLINDRICAL_SURFACE('',#4645,0.0045);
#354=CIRCLE('',#4598,0.031);
#355=CIRCLE('',#4599,0.031);
#356=CIRCLE('',#4601,0.03);
#357=CIRCLE('',#4603,0.03);
#358=CIRCLE('',#4613,0.001);
#359=CIRCLE('',#4615,0.001);
#360=CIRCLE('',#4618,0.026);
#361=CIRCLE('',#4619,0.024);
#362=CIRCLE('',#4621,0.027);
#363=CIRCLE('',#4622,0.026);
#364=CIRCLE('',#4625,0.026);
#365=CIRCLE('',#4626,0.027);
#366=CIRCLE('',#4628,0.026);
#367=CIRCLE('',#4629,0.024);
#368=CIRCLE('',#4633,0.001);
#369=CIRCLE('',#4635,0.001);
#370=CIRCLE('',#4640,0.0045);
#371=CIRCLE('',#4642,0.0045);
#372=CIRCLE('',#4644,0.0045);
#373=CIRCLE('',#4646,0.0045);
#599=B_SPLINE_CURVE_WITH_KNOTS('',3,(#6739,#6740,#6741,#6742,#6743),
 .UNSPECIFIED.,.F.,.F.,(4,1,4),(0.,0.000805913704203702,0.0016118274084074),
 .UNSPECIFIED.);
#600=B_SPLINE_CURVE_WITH_KNOTS('',3,(#6747,#6748,#6749,#6750,#6751),
 .UNSPECIFIED.,.F.,.F.,(4,1,4),(0.,0.000805913704203702,0.0016118274084074),
 .UNSPECIFIED.);
#601=B_SPLINE_CURVE_WITH_KNOTS('',3,(#6753,#6754,#6755,#6756,#6757),
 .UNSPECIFIED.,.F.,.F.,(4,1,4),(0.,0.000805913704203699,0.0016118274084074),
 .UNSPECIFIED.);
#602=B_SPLINE_CURVE_WITH_KNOTS('',3,(#6759,#6760,#6761,#6762,#6763),
 .UNSPECIFIED.,.F.,.F.,(4,1,4),(0.,0.000805913704203701,0.0016118274084074),
 .UNSPECIFIED.);
#603=B_SPLINE_CURVE_WITH_KNOTS('',3,(#6818,#6819,#6820,#6821,#6822),
 .UNSPECIFIED.,.F.,.F.,(4,1,4),(0.000383476419715099,0.0011765940099438,
0.0019697116001725),.UNSPECIFIED.);
#604=B_SPLINE_CURVE_WITH_KNOTS('',3,(#6826,#6827,#6828,#6829,#6830),
 .UNSPECIFIED.,.F.,.F.,(4,1,4),(0.00616146542423319,0.00695359511819705,
0.0077457248121609),.UNSPECIFIED.);
#605=B_SPLINE_CURVE_WITH_KNOTS('',3,(#6838,#6839,#6840,#6841,#6842),
 .UNSPECIFIED.,.F.,.F.,(4,1,4),(0.00437149970837484,0.00516403730127254,
0.00595657489417023),.UNSPECIFIED.);
#606=B_SPLINE_CURVE_WITH_KNOTS('',3,(#6846,#6847,#6848,#6849,#6850),
 .UNSPECIFIED.,.F.,.F.,(4,1,4),(0.00493537550573997,0.00572807532890887,
0.00652077515207777),.UNSPECIFIED.);
#863=ORIENTED_EDGE('',*,*,#1951,.T.);
#864=ORIENTED_EDGE('',*,*,#1952,.T.);
#865=ORIENTED_EDGE('',*,*,#1953,.F.);
#866=ORIENTED_EDGE('',*,*,#1954,.T.);
#867=ORIENTED_EDGE('',*,*,#1955,.T.);
#868=ORIENTED_EDGE('',*,*,#1956,.F.);
#869=ORIENTED_EDGE('',*,*,#1957,.F.);
#870=ORIENTED_EDGE('',*,*,#1954,.F.);
#871=ORIENTED_EDGE('',*,*,#1958,.T.);
#872=ORIENTED_EDGE('',*,*,#1952,.F.);
#873=ORIENTED_EDGE('',*,*,#1959,.F.);
#874=ORIENTED_EDGE('',*,*,#1960,.F.);
#875=ORIENTED_EDGE('',*,*,#1961,.T.);
#876=ORIENTED_EDGE('',*,*,#1962,.F.);
#877=ORIENTED_EDGE('',*,*,#1955,.F.);
#878=ORIENTED_EDGE('',*,*,#1963,.F.);
#879=ORIENTED_EDGE('',*,*,#1964,.T.);
#880=ORIENTED_EDGE('',*,*,#1965,.F.);
#881=ORIENTED_EDGE('',*,*,#1958,.F.);
#882=ORIENTED_EDGE('',*,*,#1966,.F.);
#883=ORIENTED_EDGE('',*,*,#1957,.T.);
#884=ORIENTED_EDGE('',*,*,#1967,.F.);
#885=ORIENTED_EDGE('',*,*,#1968,.F.);
#886=ORIENTED_EDGE('',*,*,#1969,.F.);
#887=ORIENTED_EDGE('',*,*,#1959,.T.);
#888=ORIENTED_EDGE('',*,*,#1970,.F.);
#889=ORIENTED_EDGE('',*,*,#1971,.F.);
#890=ORIENTED_EDGE('',*,*,#1972,.F.);
#891=ORIENTED_EDGE('',*,*,#1973,.F.);
#892=ORIENTED_EDGE('',*,*,#1974,.F.);
#893=ORIENTED_EDGE('',*,*,#1964,.F.);
#894=ORIENTED_EDGE('',*,*,#1975,.F.);
#895=ORIENTED_EDGE('',*,*,#1976,.F.);
#896=ORIENTED_EDGE('',*,*,#1977,.F.);
#897=ORIENTED_EDGE('',*,*,#1961,.F.);
#898=ORIENTED_EDGE('',*,*,#1978,.F.);
#899=ORIENTED_EDGE('',*,*,#1979,.F.);
#900=ORIENTED_EDGE('',*,*,#1978,.T.);
#901=ORIENTED_EDGE('',*,*,#1980,.F.);
#902=ORIENTED_EDGE('',*,*,#1974,.T.);
#903=ORIENTED_EDGE('',*,*,#1981,.F.);
#904=ORIENTED_EDGE('',*,*,#1982,.F.);
#905=ORIENTED_EDGE('',*,*,#1983,.F.);
#906=ORIENTED_EDGE('',*,*,#1984,.T.);
#907=ORIENTED_EDGE('',*,*,#1985,.F.);
#908=ORIENTED_EDGE('',*,*,#1986,.T.);
#909=ORIENTED_EDGE('',*,*,#1987,.F.);
#910=ORIENTED_EDGE('',*,*,#1988,.T.);
#911=ORIENTED_EDGE('',*,*,#1989,.F.);
#912=ORIENTED_EDGE('',*,*,#1987,.T.);
#913=ORIENTED_EDGE('',*,*,#1990,.F.);
#914=ORIENTED_EDGE('',*,*,#1982,.T.);
#915=ORIENTED_EDGE('',*,*,#1991,.F.);
#916=ORIENTED_EDGE('',*,*,#1992,.T.);
#917=ORIENTED_EDGE('',*,*,#1993,.F.);
#918=ORIENTED_EDGE('',*,*,#1994,.T.);
#919=ORIENTED_EDGE('',*,*,#1995,.F.);
#920=ORIENTED_EDGE('',*,*,#1996,.T.);
#921=ORIENTED_EDGE('',*,*,#1997,.F.);
#922=ORIENTED_EDGE('',*,*,#1998,.F.);
#923=ORIENTED_EDGE('',*,*,#1996,.F.);
#924=ORIENTED_EDGE('',*,*,#1999,.T.);
#925=ORIENTED_EDGE('',*,*,#1991,.T.);
#926=ORIENTED_EDGE('',*,*,#2000,.T.);
#927=ORIENTED_EDGE('',*,*,#1998,.T.);
#928=ORIENTED_EDGE('',*,*,#2001,.T.);
#929=ORIENTED_EDGE('',*,*,#1984,.F.);
#930=ORIENTED_EDGE('',*,*,#2002,.T.);
#931=ORIENTED_EDGE('',*,*,#2003,.F.);
#932=ORIENTED_EDGE('',*,*,#2004,.F.);
#933=ORIENTED_EDGE('',*,*,#1971,.T.);
#934=ORIENTED_EDGE('',*,*,#2005,.F.);
#935=ORIENTED_EDGE('',*,*,#2006,.F.);
#936=ORIENTED_EDGE('',*,*,#2007,.F.);
#937=ORIENTED_EDGE('',*,*,#1968,.T.);
#938=ORIENTED_EDGE('',*,*,#2008,.F.);
#939=ORIENTED_EDGE('',*,*,#2007,.T.);
#940=ORIENTED_EDGE('',*,*,#2009,.T.);
#941=ORIENTED_EDGE('',*,*,#2005,.T.);
#942=ORIENTED_EDGE('',*,*,#2010,.T.);
#943=ORIENTED_EDGE('',*,*,#2004,.T.);
#944=ORIENTED_EDGE('',*,*,#2011,.T.);
#945=ORIENTED_EDGE('',*,*,#1993,.T.);
#946=ORIENTED_EDGE('',*,*,#2012,.T.);
#947=ORIENTED_EDGE('',*,*,#1975,.T.);
#948=ORIENTED_EDGE('',*,*,#1966,.T.);
#949=ORIENTED_EDGE('',*,*,#1960,.T.);
#950=ORIENTED_EDGE('',*,*,#1972,.T.);
#951=ORIENTED_EDGE('',*,*,#2013,.F.);
#952=ORIENTED_EDGE('',*,*,#2008,.T.);
#953=ORIENTED_EDGE('',*,*,#1967,.T.);
#954=ORIENTED_EDGE('',*,*,#1956,.T.);
#955=ORIENTED_EDGE('',*,*,#1962,.T.);
#956=ORIENTED_EDGE('',*,*,#1977,.T.);
#957=ORIENTED_EDGE('',*,*,#2014,.F.);
#958=ORIENTED_EDGE('',*,*,#1985,.T.);
#959=ORIENTED_EDGE('',*,*,#2015,.T.);
#960=ORIENTED_EDGE('',*,*,#1953,.T.);
#961=ORIENTED_EDGE('',*,*,#1965,.T.);
#962=ORIENTED_EDGE('',*,*,#1980,.T.);
#963=ORIENTED_EDGE('',*,*,#1963,.T.);
#964=ORIENTED_EDGE('',*,*,#2016,.T.);
#965=ORIENTED_EDGE('',*,*,#2015,.F.);
#966=ORIENTED_EDGE('',*,*,#2017,.T.);
#967=ORIENTED_EDGE('',*,*,#2010,.F.);
#968=ORIENTED_EDGE('',*,*,#1970,.T.);
#969=ORIENTED_EDGE('',*,*,#1951,.F.);
#970=ORIENTED_EDGE('',*,*,#1969,.T.);
#971=ORIENTED_EDGE('',*,*,#2018,.T.);
#972=ORIENTED_EDGE('',*,*,#2017,.F.);
#973=ORIENTED_EDGE('',*,*,#2011,.F.);
#974=ORIENTED_EDGE('',*,*,#2003,.T.);
#975=ORIENTED_EDGE('',*,*,#2009,.F.);
#976=ORIENTED_EDGE('',*,*,#2006,.T.);
#977=ORIENTED_EDGE('',*,*,#2013,.T.);
#978=ORIENTED_EDGE('',*,*,#1988,.F.);
#979=ORIENTED_EDGE('',*,*,#1989,.T.);
#980=ORIENTED_EDGE('',*,*,#1981,.T.);
#981=ORIENTED_EDGE('',*,*,#2001,.F.);
#982=ORIENTED_EDGE('',*,*,#1997,.T.);
#983=ORIENTED_EDGE('',*,*,#2000,.F.);
#984=ORIENTED_EDGE('',*,*,#1994,.F.);
#985=ORIENTED_EDGE('',*,*,#2018,.F.);
#986=ORIENTED_EDGE('',*,*,#1999,.F.);
#987=ORIENTED_EDGE('',*,*,#1995,.T.);
#988=ORIENTED_EDGE('',*,*,#2002,.F.);
#989=ORIENTED_EDGE('',*,*,#1983,.T.);
#990=ORIENTED_EDGE('',*,*,#1990,.T.);
#991=ORIENTED_EDGE('',*,*,#1986,.F.);
#992=ORIENTED_EDGE('',*,*,#2014,.T.);
#993=ORIENTED_EDGE('',*,*,#1976,.T.);
#994=ORIENTED_EDGE('',*,*,#1979,.T.);
#995=ORIENTED_EDGE('',*,*,#1973,.T.);
#996=ORIENTED_EDGE('',*,*,#2012,.F.);
#997=ORIENTED_EDGE('',*,*,#1992,.F.);
#998=ORIENTED_EDGE('',*,*,#2016,.F.);
#1951=EDGE_CURVE('',#2520,#2521,#2854,.T.);
#1952=EDGE_CURVE('',#2521,#2522,#354,.T.);
#1953=EDGE_CURVE('',#2523,#2522,#2855,.T.);
#1954=EDGE_CURVE('',#2523,#2520,#355,.F.);
#1955=EDGE_CURVE('',#2523,#2524,#599,.T.);
#1956=EDGE_CURVE('',#2525,#2524,#356,.T.);
#1957=EDGE_CURVE('',#2520,#2525,#600,.T.);
#1958=EDGE_CURVE('',#2526,#2522,#601,.F.);
#1959=EDGE_CURVE('',#2527,#2521,#602,.F.);
#1960=EDGE_CURVE('',#2526,#2527,#357,.F.);
#1961=EDGE_CURVE('',#2528,#2529,#41,.T.);
#1962=EDGE_CURVE('',#2524,#2529,#2856,.F.);
#1963=EDGE_CURVE('',#2528,#2523,#2857,.T.);
#1964=EDGE_CURVE('',#2530,#2531,#42,.F.);
#1965=EDGE_CURVE('',#2522,#2531,#2858,.T.);
#1966=EDGE_CURVE('',#2530,#2526,#2859,.F.);
#1967=EDGE_CURVE('',#2532,#2525,#2860,.F.);
#1968=EDGE_CURVE('',#2533,#2532,#43,.T.);
#1969=EDGE_CURVE('',#2520,#2533,#2861,.T.);
#1970=EDGE_CURVE('',#2534,#2521,#2862,.T.);
#1971=EDGE_CURVE('',#2535,#2534,#44,.F.);
#1972=EDGE_CURVE('',#2527,#2535,#2863,.F.);
#1973=EDGE_CURVE('',#2536,#2537,#358,.F.);
#1974=EDGE_CURVE('',#2531,#2536,#2864,.F.);
#1975=EDGE_CURVE('',#2537,#2530,#2865,.T.);
#1976=EDGE_CURVE('',#2538,#2539,#359,.F.);
#1977=EDGE_CURVE('',#2529,#2538,#2866,.F.);
#1978=EDGE_CURVE('',#2539,#2528,#2867,.T.);
#1979=EDGE_CURVE('',#2539,#2536,#2868,.T.);
#1980=EDGE_CURVE('',#2531,#2528,#2869,.T.);
#1981=EDGE_CURVE('',#2540,#2541,#2870,.T.);
#1982=EDGE_CURVE('',#2542,#2540,#360,.T.);
#1983=EDGE_CURVE('',#2543,#2542,#2871,.T.);
#1984=EDGE_CURVE('',#2543,#2541,#361,.T.);
#1985=EDGE_CURVE('',#2544,#2545,#362,.F.);
#1986=EDGE_CURVE('',#2544,#2546,#603,.T.);
#1987=EDGE_CURVE('',#2547,#2546,#363,.T.);
#1988=EDGE_CURVE('',#2547,#2545,#604,.T.);
#1989=EDGE_CURVE('',#2547,#2540,#2872,.F.);
#1990=EDGE_CURVE('',#2542,#2546,#2873,.T.);
#1991=EDGE_CURVE('',#2548,#2549,#364,.F.);
#1992=EDGE_CURVE('',#2548,#2550,#605,.T.);
#1993=EDGE_CURVE('',#2551,#2550,#365,.T.);
#1994=EDGE_CURVE('',#2551,#2549,#606,.T.);
#1995=EDGE_CURVE('',#2552,#2553,#2874,.T.);
#1996=EDGE_CURVE('',#2552,#2554,#366,.T.);
#1997=EDGE_CURVE('',#2555,#2554,#2875,.T.);
#1998=EDGE_CURVE('',#2553,#2555,#367,.T.);
#1999=EDGE_CURVE('',#2552,#2548,#2876,.T.);
#2000=EDGE_CURVE('',#2549,#2554,#2877,.F.);
#2001=EDGE_CURVE('',#2555,#2541,#2878,.F.);
#2002=EDGE_CURVE('',#2543,#2553,#2879,.T.);
#2003=EDGE_CURVE('',#2556,#2557,#368,.F.);
#2004=EDGE_CURVE('',#2535,#2556,#2880,.F.);
#2005=EDGE_CURVE('',#2557,#2534,#2881,.T.);
#2006=EDGE_CURVE('',#2558,#2559,#369,.F.);
#2007=EDGE_CURVE('',#2533,#2558,#2882,.F.);
#2008=EDGE_CURVE('',#2559,#2532,#2883,.T.);
#2009=EDGE_CURVE('',#2558,#2557,#2884,.T.);
#2010=EDGE_CURVE('',#2534,#2533,#2885,.T.);
#2011=EDGE_CURVE('',#2556,#2551,#2886,.T.);
#2012=EDGE_CURVE('',#2550,#2537,#2887,.T.);
#2013=EDGE_CURVE('',#2559,#2545,#2888,.T.);
#2014=EDGE_CURVE('',#2544,#2538,#2889,.T.);
#2015=EDGE_CURVE('',#2560,#2560,#370,.T.);
#2016=EDGE_CURVE('',#2561,#2561,#371,.F.);
#2017=EDGE_CURVE('',#2562,#2562,#372,.T.);
#2018=EDGE_CURVE('',#2563,#2563,#373,.F.);
#2520=VERTEX_POINT('',#6731);
#2521=VERTEX_POINT('',#6732);
#2522=VERTEX_POINT('',#6734);
#2523=VERTEX_POINT('',#6736);
#2524=VERTEX_POINT('',#6744);
#2525=VERTEX_POINT('',#6746);
#2526=VERTEX_POINT('',#6758);
#2527=VERTEX_POINT('',#6764);
#2528=VERTEX_POINT('',#6768);
#2529=VERTEX_POINT('',#6769);
#2530=VERTEX_POINT('',#6774);
#2531=VERTEX_POINT('',#6775);
#2532=VERTEX_POINT('',#6780);
#2533=VERTEX_POINT('',#6782);
#2534=VERTEX_POINT('',#6786);
#2535=VERTEX_POINT('',#6788);
#2536=VERTEX_POINT('',#6792);
#2537=VERTEX_POINT('',#6793);
#2538=VERTEX_POINT('',#6798);
#2539=VERTEX_POINT('',#6799);
#2540=VERTEX_POINT('',#6807);
#2541=VERTEX_POINT('',#6808);
#2542=VERTEX_POINT('',#6810);
#2543=VERTEX_POINT('',#6812);
#2544=VERTEX_POINT('',#6816);
#2545=VERTEX_POINT('',#6817);
#2546=VERTEX_POINT('',#6823);
#2547=VERTEX_POINT('',#6825);
#2548=VERTEX_POINT('',#6836);
#2549=VERTEX_POINT('',#6837);
#2550=VERTEX_POINT('',#6843);
#2551=VERTEX_POINT('',#6845);
#2552=VERTEX_POINT('',#6853);
#2553=VERTEX_POINT('',#6854);
#2554=VERTEX_POINT('',#6856);
#2555=VERTEX_POINT('',#6858);
#2556=VERTEX_POINT('',#6868);
#2557=VERTEX_POINT('',#6869);
#2558=VERTEX_POINT('',#6874);
#2559=VERTEX_POINT('',#6875);
#2560=VERTEX_POINT('',#6889);
#2561=VERTEX_POINT('',#6892);
#2562=VERTEX_POINT('',#6895);
#2563=VERTEX_POINT('',#6898);
#2854=LINE('',#6730,#3032);
#2855=LINE('',#6735,#3033);
#2856=LINE('',#6770,#3034);
#2857=LINE('',#6771,#3035);
#2858=LINE('',#6776,#3036);
#2859=LINE('',#6777,#3037);
#2860=LINE('',#6779,#3038);
#2861=LINE('',#6783,#3039);
#2862=LINE('',#6785,#3040);
#2863=LINE('',#6789,#3041);
#2864=LINE('',#6794,#3042);
#2865=LINE('',#6795,#3043);
#2866=LINE('',#6800,#3044);
#2867=LINE('',#6801,#3045);
#2868=LINE('',#6803,#3046);
#2869=LINE('',#6804,#3047);
#2870=LINE('',#6806,#3048);
#2871=LINE('',#6811,#3049);
#2872=LINE('',#6832,#3050);
#2873=LINE('',#6833,#3051);
#2874=LINE('',#6852,#3052);
#2875=LINE('',#6857,#3053);
#2876=LINE('',#6861,#3054);
#2877=LINE('',#6862,#3055);
#2878=LINE('',#6864,#3056);
#2879=LINE('',#6865,#3057);
#2880=LINE('',#6870,#3058);
#2881=LINE('',#6871,#3059);
#2882=LINE('',#6876,#3060);
#2883=LINE('',#6877,#3061);
#2884=LINE('',#6879,#3062);
#2885=LINE('',#6880,#3063);
#2886=LINE('',#6882,#3064);
#2887=LINE('',#6883,#3065);
#2888=LINE('',#6885,#3066);
#2889=LINE('',#6886,#3067);
#3032=VECTOR('',#5312,1.);
#3033=VECTOR('',#5315,1.);
#3034=VECTOR('',#5330,1.);
#3035=VECTOR('',#5331,1.);
#3036=VECTOR('',#5336,1.);
#3037=VECTOR('',#5337,1.);
#3038=VECTOR('',#5340,1.);
#3039=VECTOR('',#5343,1.);
#3040=VECTOR('',#5346,1.);
#3041=VECTOR('',#5349,1.);
#3042=VECTOR('',#5354,1.);
#3043=VECTOR('',#5355,1.);
#3044=VECTOR('',#5360,1.);
#3045=VECTOR('',#5361,1.);
#3046=VECTOR('',#5364,1.);
#3047=VECTOR('',#5365,1.);
#3048=VECTOR('',#5368,1.);
#3049=VECTOR('',#5371,1.);
#3050=VECTOR('',#5382,1.);
#3051=VECTOR('',#5383,1.);
#3052=VECTOR('',#5392,1.);
#3053=VECTOR('',#5395,1.);
#3054=VECTOR('',#5400,1.);
#3055=VECTOR('',#5401,1.);
#3056=VECTOR('',#5404,1.);
#3057=VECTOR('',#5405,1.);
#3058=VECTOR('',#5410,1.);
#3059=VECTOR('',#5411,1.);
#3060=VECTOR('',#5416,1.);
#3061=VECTOR('',#5417,1.);
#3062=VECTOR('',#5420,1.);
#3063=VECTOR('',#5421,1.);
#3064=VECTOR('',#5424,1.);
#3065=VECTOR('',#5425,1.);
#3066=VECTOR('',#5428,1.);
#3067=VECTOR('',#5429,1.);
#3290=EDGE_LOOP('',(#863,#864,#865,#866));
#3291=EDGE_LOOP('',(#867,#868,#869,#870));
#3292=EDGE_LOOP('',(#871,#872,#873,#874));
#3293=EDGE_LOOP('',(#875,#876,#877,#878));
#3294=EDGE_LOOP('',(#879,#880,#881,#882));
#3295=EDGE_LOOP('',(#883,#884,#885,#886));
#3296=EDGE_LOOP('',(#887,#888,#889,#890));
#3297=EDGE_LOOP('',(#891,#892,#893,#894));
#3298=EDGE_LOOP('',(#895,#896,#897,#898));
#3299=EDGE_LOOP('',(#899,#900,#901,#902));
#3300=EDGE_LOOP('',(#903,#904,#905,#906));
#3301=EDGE_LOOP('',(#907,#908,#909,#910));
#3302=EDGE_LOOP('',(#911,#912,#913,#914));
#3303=EDGE_LOOP('',(#915,#916,#917,#918));
#3304=EDGE_LOOP('',(#919,#920,#921,#922));
#3305=EDGE_LOOP('',(#923,#924,#925,#926));
#3306=EDGE_LOOP('',(#927,#928,#929,#930));
#3307=EDGE_LOOP('',(#931,#932,#933,#934));
#3308=EDGE_LOOP('',(#935,#936,#937,#938));
#3309=EDGE_LOOP('',(#939,#940,#941,#942));
#3310=EDGE_LOOP('',(#943,#944,#945,#946,#947,#948,#949,#950));
#3311=EDGE_LOOP('',(#951,#952,#953,#954,#955,#956,#957,#958));
#3312=EDGE_LOOP('',(#959));
#3313=EDGE_LOOP('',(#960,#961,#962,#963));
#3314=EDGE_LOOP('',(#964));
#3315=EDGE_LOOP('',(#965));
#3316=EDGE_LOOP('',(#966));
#3317=EDGE_LOOP('',(#967,#968,#969,#970));
#3318=EDGE_LOOP('',(#971));
#3319=EDGE_LOOP('',(#972));
#3320=EDGE_LOOP('',(#973,#974,#975,#976,#977,#978,#979,#980,#981,#982,#983,
#984));
#3321=EDGE_LOOP('',(#985));
#3322=EDGE_LOOP('',(#986,#987,#988,#989,#990,#991,#992,#993,#994,#995,#996,
#997));
#3323=EDGE_LOOP('',(#998));
#3667=FACE_BOUND('',#3290,.T.);
#3668=FACE_BOUND('',#3291,.T.);
#3669=FACE_BOUND('',#3292,.T.);
#3670=FACE_BOUND('',#3293,.T.);
#3671=FACE_BOUND('',#3294,.T.);
#3672=FACE_BOUND('',#3295,.T.);
#3673=FACE_BOUND('',#3296,.T.);
#3674=FACE_BOUND('',#3297,.T.);
#3675=FACE_BOUND('',#3298,.T.);
#3676=FACE_BOUND('',#3299,.T.);
#3677=FACE_BOUND('',#3300,.T.);
#3678=FACE_BOUND('',#3301,.T.);
#3679=FACE_BOUND('',#3302,.T.);
#3680=FACE_BOUND('',#3303,.T.);
#3681=FACE_BOUND('',#3304,.T.);
#3682=FACE_BOUND('',#3305,.T.);
#3683=FACE_BOUND('',#3306,.T.);
#3684=FACE_BOUND('',#3307,.T.);
#3685=FACE_BOUND('',#3308,.T.);
#3686=FACE_BOUND('',#3309,.T.);
#3687=FACE_BOUND('',#3310,.T.);
#3688=FACE_BOUND('',#3311,.T.);
#3689=FACE_BOUND('',#3312,.T.);
#3690=FACE_BOUND('',#3313,.T.);
#3691=FACE_BOUND('',#3314,.T.);
#3692=FACE_BOUND('',#3315,.T.);
#3693=FACE_BOUND('',#3316,.T.);
#3694=FACE_BOUND('',#3317,.T.);
#3695=FACE_BOUND('',#3318,.T.);
#3696=FACE_BOUND('',#3319,.T.);
#3697=FACE_BOUND('',#3320,.T.);
#3698=FACE_BOUND('',#3321,.T.);
#3699=FACE_BOUND('',#3322,.T.);
#3700=FACE_BOUND('',#3323,.T.);
#3974=PLANE('',#4616);
#3975=PLANE('',#4617);
#3976=PLANE('',#4627);
#3977=PLANE('',#4636);
#3978=PLANE('',#4637);
#3979=PLANE('',#4638);
#3980=PLANE('',#4639);
#3981=PLANE('',#4643);
#3982=PLANE('',#4647);
#3983=PLANE('',#4648);
#4095=ADVANCED_FACE('',(#3667),#225,.T.);
#4096=ADVANCED_FACE('',(#3668),#140,.T.);
#4097=ADVANCED_FACE('',(#3669),#141,.T.);
#4098=ADVANCED_FACE('',(#3670),#226,.T.);
#4099=ADVANCED_FACE('',(#3671),#227,.T.);
#4100=ADVANCED_FACE('',(#3672),#228,.T.);
#4101=ADVANCED_FACE('',(#3673),#229,.T.);
#4102=ADVANCED_FACE('',(#3674),#230,.T.);
#4103=ADVANCED_FACE('',(#3675),#231,.T.);
#4104=ADVANCED_FACE('',(#3676),#3974,.T.);
#4105=ADVANCED_FACE('',(#3677),#3975,.T.);
#4106=ADVANCED_FACE('',(#3678),#142,.F.);
#4107=ADVANCED_FACE('',(#3679),#232,.T.);
#4108=ADVANCED_FACE('',(#3680),#143,.F.);
#4109=ADVANCED_FACE('',(#3681),#3976,.T.);
#4110=ADVANCED_FACE('',(#3682),#233,.T.);
#4111=ADVANCED_FACE('',(#3683),#234,.F.);
#4112=ADVANCED_FACE('',(#3684),#235,.T.);
#4113=ADVANCED_FACE('',(#3685),#236,.T.);
#4114=ADVANCED_FACE('',(#3686),#3977,.F.);
#4115=ADVANCED_FACE('',(#3687),#3978,.F.);
#4116=ADVANCED_FACE('',(#3688),#3979,.T.);
#4117=ADVANCED_FACE('',(#3689,#3690),#3980,.F.);
#4118=ADVANCED_FACE('',(#3691,#3692),#237,.F.);
#4119=ADVANCED_FACE('',(#3693,#3694),#3981,.F.);
#4120=ADVANCED_FACE('',(#3695,#3696),#238,.F.);
#4121=ADVANCED_FACE('',(#3697,#3698),#3982,.F.);
#4122=ADVANCED_FACE('',(#3699,#3700),#3983,.F.);
#4328=CLOSED_SHELL('',(#4095,#4096,#4097,#4098,#4099,#4100,#4101,#4102,
#4103,#4104,#4105,#4106,#4107,#4108,#4109,#4110,#4111,#4112,#4113,#4114,
#4115,#4116,#4117,#4118,#4119,#4120,#4121,#4122));
#4339=STYLED_ITEM('',(#4350),#4454);
#4350=PRESENTATION_STYLE_ASSIGNMENT((#4366));
#4366=SURFACE_STYLE_USAGE(.BOTH.,#4382);
#4382=SURFACE_SIDE_STYLE('',(#4398));
#4398=SURFACE_STYLE_FILL_AREA(#4414);
#4414=FILL_AREA_STYLE('',(#4430));
#4430=FILL_AREA_STYLE_COLOUR('',#4442);
#4442=COLOUR_RGB('', 0.31764706, 0.68627451, 0.89019608);
#4454=MANIFOLD_SOLID_BREP('Part 2',#4328);
#4466=SHAPE_DEFINITION_REPRESENTATION(#8575,#4478);
#4478=SHAPE_REPRESENTATION('Part 2',(#4484),#8541);
#4484=AXIS2_PLACEMENT_3D('',#6402,#5064,#5065);
#4597=AXIS2_PLACEMENT_3D('',#6729,#5310,#5311);
#4598=AXIS2_PLACEMENT_3D('',#6733,#5313,#5314);
#4599=AXIS2_PLACEMENT_3D('',#6737,#5316,#5317);
#4600=AXIS2_PLACEMENT_3D('',#6738,#5318,#5319);
#4601=AXIS2_PLACEMENT_3D('',#6745,#5320,#5321);
#4602=AXIS2_PLACEMENT_3D('',#6752,#5322,#5323);
#4603=AXIS2_PLACEMENT_3D('',#6765,#5324,#5325);
#4604=AXIS2_PLACEMENT_3D('',#6766,#5326,#5327);
#4605=AXIS2_PLACEMENT_3D('',#6767,#5328,#5329);
#4606=AXIS2_PLACEMENT_3D('',#6772,#5332,#5333);
#4607=AXIS2_PLACEMENT_3D('',#6773,#5334,#5335);
#4608=AXIS2_PLACEMENT_3D('',#6778,#5338,#5339);
#4609=AXIS2_PLACEMENT_3D('',#6781,#5341,#5342);
#4610=AXIS2_PLACEMENT_3D('',#6784,#5344,#5345);
#4611=AXIS2_PLACEMENT_3D('',#6787,#5347,#5348);
#4612=AXIS2_PLACEMENT_3D('',#6790,#5350,#5351);
#4613=AXIS2_PLACEMENT_3D('',#6791,#5352,#5353);
#4614=AXIS2_PLACEMENT_3D('',#6796,#5356,#5357);
#4615=AXIS2_PLACEMENT_3D('',#6797,#5358,#5359);
#4616=AXIS2_PLACEMENT_3D('',#6802,#5362,#5363);
#4617=AXIS2_PLACEMENT_3D('',#6805,#5366,#5367);
#4618=AXIS2_PLACEMENT_3D('',#6809,#5369,#5370);
#4619=AXIS2_PLACEMENT_3D('',#6813,#5372,#5373);
#4620=AXIS2_PLACEMENT_3D('',#6814,#5374,#5375);
#4621=AXIS2_PLACEMENT_3D('',#6815,#5376,#5377);
#4622=AXIS2_PLACEMENT_3D('',#6824,#5378,#5379);
#4623=AXIS2_PLACEMENT_3D('',#6831,#5380,#5381);
#4624=AXIS2_PLACEMENT_3D('',#6834,#5384,#5385);
#4625=AXIS2_PLACEMENT_3D('',#6835,#5386,#5387);
#4626=AXIS2_PLACEMENT_3D('',#6844,#5388,#5389);
#4627=AXIS2_PLACEMENT_3D('',#6851,#5390,#5391);
#4628=AXIS2_PLACEMENT_3D('',#6855,#5393,#5394);
#4629=AXIS2_PLACEMENT_3D('',#6859,#5396,#5397);
#4630=AXIS2_PLACEMENT_3D('',#6860,#5398,#5399);
#4631=AXIS2_PLACEMENT_3D('',#6863,#5402,#5403);
#4632=AXIS2_PLACEMENT_3D('',#6866,#5406,#5407);
#4633=AXIS2_PLACEMENT_3D('',#6867,#5408,#5409);
#4634=AXIS2_PLACEMENT_3D('',#6872,#5412,#5413);
#4635=AXIS2_PLACEMENT_3D('',#6873,#5414,#5415);
#4636=AXIS2_PLACEMENT_3D('',#6878,#5418,#5419);
#4637=AXIS2_PLACEMENT_3D('',#6881,#5422,#5423);
#4638=AXIS2_PLACEMENT_3D('',#6884,#5426,#5427);
#4639=AXIS2_PLACEMENT_3D('',#6887,#5430,#5431);
#4640=AXIS2_PLACEMENT_3D('',#6888,#5432,#5433);
#4641=AXIS2_PLACEMENT_3D('',#6890,#5434,#5435);
#4642=AXIS2_PLACEMENT_3D('',#6891,#5436,#5437);
#4643=AXIS2_PLACEMENT_3D('',#6893,#5438,#5439);
#4644=AXIS2_PLACEMENT_3D('',#6894,#5440,#5441);
#4645=AXIS2_PLACEMENT_3D('',#6896,#5442,#5443);
#4646=AXIS2_PLACEMENT_3D('',#6897,#5444,#5445);
#4647=AXIS2_PLACEMENT_3D('',#6899,#5446,#5447);
#4648=AXIS2_PLACEMENT_3D('',#6900,#5448,#5449);
#5064=DIRECTION('',(0.,0.,1.));
#5065=DIRECTION('',(1.,0.,0.));
#5310=DIRECTION('',(0.,0.,1.));
#5311=DIRECTION('',(1.,0.,0.));
#5312=DIRECTION('',(0.,0.,1.));
#5313=DIRECTION('',(0.,1.11917643611407E-16,-1.));
#5314=DIRECTION('',(0.,1.,1.11917643611407E-16));
#5315=DIRECTION('',(0.,0.,1.));
#5316=DIRECTION('',(0.,1.11917643611407E-16,-1.));
#5317=DIRECTION('',(0.,1.,1.11917643611407E-16));
#5318=DIRECTION('',(0.,1.11917643611407E-16,-1.));
#5319=DIRECTION('',(0.,1.,1.11917643611407E-16));
#5320=DIRECTION('',(0.,1.11917643611407E-16,-1.));
#5321=DIRECTION('',(0.,1.,1.11917643611407E-16));
#5322=DIRECTION('',(0.,1.11917643611407E-16,-1.));
#5323=DIRECTION('',(0.,1.,1.11917643611407E-16));
#5324=DIRECTION('',(0.,1.11917643611407E-16,-1.));
#5325=DIRECTION('',(0.,1.,1.11917643611407E-16));
#5326=DIRECTION('',(-1.,-3.90153196957302E-16,-4.36650264509183E-32));
#5327=DIRECTION('',(3.90153196957302E-16,-1.,0.));
#5328=DIRECTION('',(0.707106781186548,-0.707106781186548,-7.91377247320451E-17));
#5329=DIRECTION('',(-0.707106781186548,-0.707106781186548,-7.91377247320451E-17));
#5330=DIRECTION('',(1.,3.90153196957302E-16,4.36650264509183E-32));
#5331=DIRECTION('',(1.,3.90153196957302E-16,4.36650264509183E-32));
#5332=DIRECTION('',(-1.,-3.90153196957302E-16,-4.36650264509183E-32));
#5333=DIRECTION('',(3.90153196957302E-16,-1.,0.));
#5334=DIRECTION('',(-0.707106781186548,0.707106781186548,7.91377247320451E-17));
#5335=DIRECTION('',(0.707106781186548,0.707106781186548,7.91377247320451E-17));
#5336=DIRECTION('',(-1.,-3.90153196957302E-16,-4.36650264509183E-32));
#5337=DIRECTION('',(-1.,-3.90153196957302E-16,-4.36650264509183E-32));
#5338=DIRECTION('',(-1.,0.,0.));
#5339=DIRECTION('',(0.,0.,1.));
#5340=DIRECTION('',(1.,0.,0.));
#5341=DIRECTION('',(0.707106781186548,0.707106781186548,7.91377247320451E-17));
#5342=DIRECTION('',(-0.707106781186548,0.707106781186548,7.91377247320451E-17));
#5343=DIRECTION('',(1.,0.,0.));
#5344=DIRECTION('',(-1.,0.,0.));
#5345=DIRECTION('',(0.,0.,1.));
#5346=DIRECTION('',(-1.,0.,0.));
#5347=DIRECTION('',(-0.707106781186548,-0.707106781186548,-7.91377247320451E-17));
#5348=DIRECTION('',(0.707106781186548,-0.707106781186548,-7.91377247320451E-17));
#5349=DIRECTION('',(-1.,0.,0.));
#5350=DIRECTION('',(0.,1.,1.11917643611407E-16));
#5351=DIRECTION('',(0.,-1.11917643611407E-16,1.));
#5352=DIRECTION('',(0.,-1.,0.));
#5353=DIRECTION('',(0.,0.,-1.));
#5354=DIRECTION('',(0.,-1.,-1.11917643611407E-16));
#5355=DIRECTION('',(0.,-1.,-1.11917643611407E-16));
#5356=DIRECTION('',(0.,-1.,-1.11917643611407E-16));
#5357=DIRECTION('',(0.,1.11917643611407E-16,-1.));
#5358=DIRECTION('',(0.,-1.,0.));
#5359=DIRECTION('',(0.,0.,-1.));
#5360=DIRECTION('',(0.,-1.,-1.11917643611407E-16));
#5361=DIRECTION('',(0.,-1.,-1.11917643611407E-16));
#5362=DIRECTION('',(-1.,0.,0.));
#5363=DIRECTION('',(0.,0.,1.));
#5364=DIRECTION('',(0.,0.,1.));
#5365=DIRECTION('',(0.,0.,-1.));
#5366=DIRECTION('',(0.,0.,-1.));
#5367=DIRECTION('',(1.,0.,0.));
#5368=DIRECTION('',(-1.,0.,0.));
#5369=DIRECTION('',(0.,0.,1.));
#5370=DIRECTION('',(1.,0.,0.));
#5371=DIRECTION('',(-1.,0.,0.));
#5372=DIRECTION('',(0.,0.,1.));
#5373=DIRECTION('',(1.,0.,0.));
#5374=DIRECTION('',(0.,1.11917643611407E-16,-1.));
#5375=DIRECTION('',(0.,1.,1.11917643611407E-16));
#5376=DIRECTION('',(0.,1.11917643611407E-16,-1.));
#5377=DIRECTION('',(0.,1.,1.11917643611407E-16));
#5378=DIRECTION('',(0.,1.11917643611407E-16,-1.));
#5379=DIRECTION('',(0.,1.,1.11917643611407E-16));
#5380=DIRECTION('',(0.,0.,1.));
#5381=DIRECTION('',(1.,0.,0.));
#5382=DIRECTION('',(0.,0.,1.));
#5383=DIRECTION('',(0.,0.,1.));
#5384=DIRECTION('',(0.,1.11917643611407E-16,-1.));
#5385=DIRECTION('',(0.,1.,1.11917643611407E-16));
#5386=DIRECTION('',(0.,1.11917643611407E-16,-1.));
#5387=DIRECTION('',(0.,1.,1.11917643611407E-16));
#5388=DIRECTION('',(0.,1.11917643611407E-16,-1.));
#5389=DIRECTION('',(0.,1.,1.11917643611407E-16));
#5390=DIRECTION('',(0.,0.,1.));
#5391=DIRECTION('',(1.,0.,0.));
#5392=DIRECTION('',(1.,0.,0.));
#5393=DIRECTION('',(0.,0.,1.));
#5394=DIRECTION('',(1.,0.,0.));
#5395=DIRECTION('',(1.,0.,0.));
#5396=DIRECTION('',(0.,0.,1.));
#5397=DIRECTION('',(1.,0.,0.));
#5398=DIRECTION('',(0.,0.,-1.));
#5399=DIRECTION('',(-1.,0.,0.));
#5400=DIRECTION('',(0.,0.,-1.));
#5401=DIRECTION('',(0.,0.,-1.));
#5402=DIRECTION('',(0.,0.,1.));
#5403=DIRECTION('',(1.,0.,0.));
#5404=DIRECTION('',(0.,0.,1.));
#5405=DIRECTION('',(0.,0.,1.));
#5406=DIRECTION('',(0.,-1.,-1.11917643611407E-16));
#5407=DIRECTION('',(0.,1.11917643611407E-16,-1.));
#5408=DIRECTION('',(0.,-1.,0.));
#5409=DIRECTION('',(0.,0.,-1.));
#5410=DIRECTION('',(0.,-1.,-1.11917643611407E-16));
#5411=DIRECTION('',(0.,-1.,-1.11917643611407E-16));
#5412=DIRECTION('',(0.,1.,1.11917643611407E-16));
#5413=DIRECTION('',(0.,-1.11917643611407E-16,1.));
#5414=DIRECTION('',(0.,-1.,0.));
#5415=DIRECTION('',(0.,0.,-1.));
#5416=DIRECTION('',(0.,-1.,-1.11917643611407E-16));
#5417=DIRECTION('',(0.,-1.,-1.11917643611407E-16));
#5418=DIRECTION('',(-1.,0.,0.));
#5419=DIRECTION('',(0.,0.,1.));
#5420=DIRECTION('',(0.,0.,1.));
#5421=DIRECTION('',(0.,0.,-1.));
#5422=DIRECTION('',(0.,1.11917643611407E-16,-1.));
#5423=DIRECTION('',(0.,1.,1.11917643611407E-16));
#5424=DIRECTION('',(-1.,0.,0.));
#5425=DIRECTION('',(-1.,0.,0.));
#5426=DIRECTION('',(0.,1.11917643611407E-16,-1.));
#5427=DIRECTION('',(0.,1.,1.11917643611407E-16));
#5428=DIRECTION('',(-1.,0.,0.));
#5429=DIRECTION('',(-1.,0.,0.));
#5430=DIRECTION('',(-3.90153196957302E-16,1.,0.));
#5431=DIRECTION('',(-1.,-3.90153196957302E-16,0.));
#5432=DIRECTION('',(-3.90153196957302E-16,1.,0.));
#5433=DIRECTION('',(-1.,-3.90153196957302E-16,0.));
#5434=DIRECTION('',(0.,1.,0.));
#5435=DIRECTION('',(0.,0.,1.));
#5436=DIRECTION('',(0.,-1.,0.));
#5437=DIRECTION('',(0.,0.,-1.));
#5438=DIRECTION('',(0.,1.,0.));
#5439=DIRECTION('',(0.,0.,1.));
#5440=DIRECTION('',(0.,1.,0.));
#5441=DIRECTION('',(0.,0.,1.));
#5442=DIRECTION('',(0.,1.,0.));
#5443=DIRECTION('',(0.,0.,1.));
#5444=DIRECTION('',(0.,-1.,0.));
#5445=DIRECTION('',(0.,0.,-1.));
#5446=DIRECTION('',(0.,-1.,0.));
#5447=DIRECTION('',(1.,0.,0.));
#5448=DIRECTION('',(0.,-1.,0.));
#5449=DIRECTION('',(1.,0.,0.));
#6402=CARTESIAN_POINT('',(0.,0.,0.));
#6729=CARTESIAN_POINT('',(0.,-0.0684221052,-0.0669999996));
#6730=CARTESIAN_POINT('',(0.0196214168703486,-0.0924221052,-0.0669999996));
#6731=CARTESIAN_POINT('',(0.0196214168703486,-0.0924221052,-0.0100000004));
#6732=CARTESIAN_POINT('',(0.0196214168703486,-0.0924221052,0.0100000004));
#6733=CARTESIAN_POINT('',(0.,-0.0684221052,0.0100000004));
#6734=CARTESIAN_POINT('',(-0.0196214168703486,-0.0924221052,0.0100000004));
#6735=CARTESIAN_POINT('',(-0.0196214168703486,-0.0924221052,-0.0669999996));
#6736=CARTESIAN_POINT('',(-0.0196214168703486,-0.0924221052,-0.0100000004));
#6737=CARTESIAN_POINT('',(0.,-0.0684221052,-0.0100000004));
#6738=CARTESIAN_POINT('',(0.,-0.0684221052,-0.0100000004));
#6739=CARTESIAN_POINT('',(-0.0196214168703486,-0.0924221052,-0.0100000004));
#6740=CARTESIAN_POINT('',(-0.0196214168703486,-0.0924221052,-0.0102726071240878));
#6741=CARTESIAN_POINT('',(-0.0195383172075569,-0.0921885784050125,-0.0107990864640417));
#6742=CARTESIAN_POINT('',(-0.0193531124817403,-0.0916745903152378,-0.0110000004));
#6743=CARTESIAN_POINT('',(-0.0192613602842582,-0.0914221052,-0.0110000004));
#6744=CARTESIAN_POINT('',(-0.0192613602842583,-0.0914221052,-0.0110000004));
#6745=CARTESIAN_POINT('',(0.,-0.0684221052,-0.0110000004));
#6746=CARTESIAN_POINT('',(0.0192613602842582,-0.0914221052,-0.0110000004));
#6747=CARTESIAN_POINT('',(0.0196214168703486,-0.0924221052,-0.0100000004));
#6748=CARTESIAN_POINT('',(0.0196214168703486,-0.0924221052,-0.0102726071240878));
#6749=CARTESIAN_POINT('',(0.0195383172075569,-0.0921885784050125,-0.0107990864640417));
#6750=CARTESIAN_POINT('',(0.0193531124817403,-0.0916745903152378,-0.0110000004));
#6751=CARTESIAN_POINT('',(0.0192613602842582,-0.0914221052,-0.0110000004));
#6752=CARTESIAN_POINT('',(0.,-0.0684221052,0.0100000004));
#6753=CARTESIAN_POINT('',(-0.0196214168703486,-0.0924221052,0.0100000004));
#6754=CARTESIAN_POINT('',(-0.0196214168703486,-0.0924221052,0.0102726071240878));
#6755=CARTESIAN_POINT('',(-0.0195383172075741,-0.0921885784050062,0.0107990864640417));
#6756=CARTESIAN_POINT('',(-0.0193531124817059,-0.0916745903152503,0.0110000004));
#6757=CARTESIAN_POINT('',(-0.0192613602842582,-0.0914221052,0.0110000004));
#6758=CARTESIAN_POINT('',(-0.0192613602842582,-0.0914221052,0.0110000004));
#6759=CARTESIAN_POINT('',(0.0196214168703486,-0.0924221052,0.0100000004));
#6760=CARTESIAN_POINT('',(0.0196214168703486,-0.0924221052,0.0102726071240878));
#6761=CARTESIAN_POINT('',(0.0195383172075741,-0.0921885784050062,0.0107990864640417));
#6762=CARTESIAN_POINT('',(0.0193531124817059,-0.0916745903152503,0.0110000004));
#6763=CARTESIAN_POINT('',(0.0192613602842582,-0.0914221052,0.0110000004));
#6764=CARTESIAN_POINT('',(0.0192613602842582,-0.0914221052,0.0110000004));
#6765=CARTESIAN_POINT('',(0.,-0.0684221052,0.0110000004));
#6766=CARTESIAN_POINT('',(-0.0196214168703486,-0.0914221052,-0.0100000004));
#6767=CARTESIAN_POINT('',(-0.03550000008,-0.0914221052,-0.0100000004));
#6768=CARTESIAN_POINT('',(-0.03650000008,-0.0924221052,-0.0100000004));
#6769=CARTESIAN_POINT('',(-0.03550000008,-0.0914221052,-0.0110000004));
#6770=CARTESIAN_POINT('',(-0.03650000008,-0.0914221052,-0.0110000004));
#6771=CARTESIAN_POINT('',(-0.0196214168703486,-0.0924221052,-0.0100000004));
#6772=CARTESIAN_POINT('',(-0.0196214168703486,-0.0914221052,0.0100000004));
#6773=CARTESIAN_POINT('',(-0.03550000008,-0.0914221052,0.0100000004));
#6774=CARTESIAN_POINT('',(-0.03550000008,-0.0914221052,0.0110000004));
#6775=CARTESIAN_POINT('',(-0.03650000008,-0.0924221052,0.0100000004));
#6776=CARTESIAN_POINT('',(-0.0196214168703486,-0.0924221052,0.0100000004));
#6777=CARTESIAN_POINT('',(0.03650000008,-0.0914221051999999,0.0110000004));
#6778=CARTESIAN_POINT('',(0.0469715027961281,-0.0914221052,-0.0100000004));
#6779=CARTESIAN_POINT('',(0.0196214168703486,-0.0914221052,-0.0110000004));
#6780=CARTESIAN_POINT('',(0.03550000008,-0.0914221052,-0.0110000004));
#6781=CARTESIAN_POINT('',(0.03550000008,-0.0914221052,-0.0100000004));
#6782=CARTESIAN_POINT('',(0.03650000008,-0.0924221052,-0.0100000004));
#6783=CARTESIAN_POINT('',(0.03650000008,-0.0924221052,-0.0100000004));
#6784=CARTESIAN_POINT('',(0.0469715027961281,-0.0914221052,0.0100000004));
#6785=CARTESIAN_POINT('',(0.0469715027961281,-0.0924221052,0.0100000004));
#6786=CARTESIAN_POINT('',(0.03650000008,-0.0924221052,0.0100000004));
#6787=CARTESIAN_POINT('',(0.03550000008,-0.0914221052,0.0100000004));
#6788=CARTESIAN_POINT('',(0.03550000008,-0.0914221052,0.0110000004));
#6789=CARTESIAN_POINT('',(0.03650000008,-0.0914221052,0.0110000004));
#6790=CARTESIAN_POINT('',(-0.03550000008,-0.0374221052,0.0100000004));
#6791=CARTESIAN_POINT('',(-0.03550000008,-0.0746532949430514,0.0100000004));
#6792=CARTESIAN_POINT('',(-0.03650000008,-0.0746532949430514,0.0100000004));
#6793=CARTESIAN_POINT('',(-0.03550000008,-0.0746532949430514,0.0110000004));
#6794=CARTESIAN_POINT('',(-0.03650000008,-0.0582659958948477,0.0100000004));
#6795=CARTESIAN_POINT('',(-0.03550000008,-0.0924221052,0.0110000004));
#6796=CARTESIAN_POINT('',(-0.03550000008,1.11917648088112E-18,-0.0100000004));
#6797=CARTESIAN_POINT('',(-0.03550000008,-0.0746532949430514,-0.0100000004));
#6798=CARTESIAN_POINT('',(-0.03550000008,-0.0746532949430514,-0.0110000004));
#6799=CARTESIAN_POINT('',(-0.03650000008,-0.0746532949430514,-0.0100000004));
#6800=CARTESIAN_POINT('',(-0.03550000008,-0.0374221052,-0.0110000004));
#6801=CARTESIAN_POINT('',(-0.03650000008,1.11917648088112E-18,-0.0100000004));
#6802=CARTESIAN_POINT('',(-0.03650000008,0.,0.));
#6803=CARTESIAN_POINT('',(-0.03650000008,-0.0746532949430514,0.));
#6804=CARTESIAN_POINT('',(-0.03650000008,-0.0924221052,0.));
#6805=CARTESIAN_POINT('',(0.,0.,-0.0130000004));
#6806=CARTESIAN_POINT('',(0.,-0.0746532949430514,-0.0130000004));
#6807=CARTESIAN_POINT('',(0.0252422715773777,-0.0746532949430514,-0.0130000004));
#6808=CARTESIAN_POINT('',(0.0231769772486856,-0.0746532949430514,-0.0130000004));
#6809=CARTESIAN_POINT('',(0.,-0.0684221052,-0.0130000004));
#6810=CARTESIAN_POINT('',(-0.0252422715773777,-0.0746532949430514,-0.0130000004));
#6811=CARTESIAN_POINT('',(0.,-0.0746532949430514,-0.0130000004));
#6812=CARTESIAN_POINT('',(-0.0231769772486856,-0.0746532949430514,-0.0130000004));
#6813=CARTESIAN_POINT('',(0.,-0.0684221052,-0.0130000004));
#6814=CARTESIAN_POINT('',(0.,-0.0684221052,-0.0120000004));
#6815=CARTESIAN_POINT('',(0.,-0.0684221052,-0.0110000004));
#6816=CARTESIAN_POINT('',(-0.0262711300553686,-0.0746532949430514,-0.0110000004));
#6817=CARTESIAN_POINT('',(0.0262711300553686,-0.0746532949430514,-0.0110000004));
#6818=CARTESIAN_POINT('',(-0.0262711300553686,-0.0746532949430514,-0.0110000004));
#6819=CARTESIAN_POINT('',(-0.0260041493105404,-0.0746532949430514,-0.0110000004));
#6820=CARTESIAN_POINT('',(-0.0254743722652179,-0.0746532949430514,-0.011208704207599));
#6821=CARTESIAN_POINT('',(-0.0252422715773777,-0.0746532949430514,-0.0117351103746111));
#6822=CARTESIAN_POINT('',(-0.0252422715773777,-0.0746532949430514,-0.0120000004));
#6823=CARTESIAN_POINT('',(-0.0252422715773777,-0.0746532949430514,-0.0120000004));
#6824=CARTESIAN_POINT('',(0.,-0.0684221052,-0.0120000004));
#6825=CARTESIAN_POINT('',(0.0252422715773777,-0.0746532949430514,-0.0120000004));
#6826=CARTESIAN_POINT('',(0.0252422715773777,-0.0746532949430514,-0.0120000004));
#6827=CARTESIAN_POINT('',(0.0252422715773777,-0.0746532949430514,-0.0117324512139406));
#6828=CARTESIAN_POINT('',(0.0254742124828446,-0.0746532949430514,-0.0112095401021891));
#6829=CARTESIAN_POINT('',(0.0260054993852186,-0.0746532949430514,-0.0110000004));
#6830=CARTESIAN_POINT('',(0.0262711300553686,-0.0746532949430514,-0.0110000004));
#6831=CARTESIAN_POINT('',(0.,-0.0684221052,-0.0130000004));
#6832=CARTESIAN_POINT('',(0.0252422715773777,-0.0746532949430514,-0.0130000004));
#6833=CARTESIAN_POINT('',(-0.0252422715773777,-0.0746532949430514,-0.0130000004));
#6834=CARTESIAN_POINT('',(0.,-0.0684221052,0.0120000004));
#6835=CARTESIAN_POINT('',(0.,-0.0684221052,0.0120000004));
#6836=CARTESIAN_POINT('',(-0.0252422715773777,-0.0746532949430514,0.0120000004));
#6837=CARTESIAN_POINT('',(0.0252422715773777,-0.0746532949430514,0.0120000004));
#6838=CARTESIAN_POINT('',(-0.0252422715773777,-0.0746532949430514,0.0120000004));
#6839=CARTESIAN_POINT('',(-0.0252422715773777,-0.0746532949430514,0.0117340892011008));
#6840=CARTESIAN_POINT('',(-0.0254741318712697,-0.0746532949430514,0.0112081301589468));
#6841=CARTESIAN_POINT('',(-0.0260068950976863,-0.0746532949430514,0.0110000004));
#6842=CARTESIAN_POINT('',(-0.0262711300553686,-0.0746532949430514,0.0110000004));
#6843=CARTESIAN_POINT('',(-0.0262711300553686,-0.0746532949430514,0.0110000004));
#6844=CARTESIAN_POINT('',(0.,-0.0684221052,0.0110000004));
#6845=CARTESIAN_POINT('',(0.0262711300553686,-0.0746532949430514,0.0110000004));
#6846=CARTESIAN_POINT('',(0.0262711300553686,-0.0746532949430514,0.0110000004));
#6847=CARTESIAN_POINT('',(0.0260068432764003,-0.0746532949430514,0.0110000004));
#6848=CARTESIAN_POINT('',(0.0254746601402995,-0.0746532949430514,0.0112068289794583));
#6849=CARTESIAN_POINT('',(0.0252422715773777,-0.0746532949430514,0.0117357303784197));
#6850=CARTESIAN_POINT('',(0.0252422715773777,-0.0746532949430514,0.0120000004));
#6851=CARTESIAN_POINT('',(0.,0.,0.0130000004));
#6852=CARTESIAN_POINT('',(0.,-0.0746532949430514,0.0130000004));
#6853=CARTESIAN_POINT('',(-0.0252422715773777,-0.0746532949430514,0.0130000004));
#6854=CARTESIAN_POINT('',(-0.0231769772486856,-0.0746532949430514,0.0130000004));
#6855=CARTESIAN_POINT('',(0.,-0.0684221052,0.0130000004));
#6856=CARTESIAN_POINT('',(0.0252422715773777,-0.0746532949430514,0.0130000004));
#6857=CARTESIAN_POINT('',(0.,-0.0746532949430514,0.0130000004));
#6858=CARTESIAN_POINT('',(0.0231769772486856,-0.0746532949430514,0.0130000004));
#6859=CARTESIAN_POINT('',(0.,-0.0684221052,0.0130000004));
#6860=CARTESIAN_POINT('',(0.,-0.0684221052,0.0130000004));
#6861=CARTESIAN_POINT('',(-0.0252422715773777,-0.0746532949430514,0.0130000004));
#6862=CARTESIAN_POINT('',(0.0252422715773777,-0.0746532949430514,0.0130000004));
#6863=CARTESIAN_POINT('',(0.,-0.0684221052,-0.01200000032));
#6864=CARTESIAN_POINT('',(0.0231769772486856,-0.0746532949430514,-0.01200000032));
#6865=CARTESIAN_POINT('',(-0.0231769772486856,-0.0746532949430514,-0.01200000032));
#6866=CARTESIAN_POINT('',(0.03550000008,-1.11917648088113E-18,0.0100000004));
#6867=CARTESIAN_POINT('',(0.03550000008,-0.0746532949430514,0.0100000004));
#6868=CARTESIAN_POINT('',(0.03550000008,-0.0746532949430514,0.0110000004));
#6869=CARTESIAN_POINT('',(0.03650000008,-0.0746532949430514,0.0100000004));
#6870=CARTESIAN_POINT('',(0.03550000008,-0.0374221052,0.0110000004));
#6871=CARTESIAN_POINT('',(0.03650000008,-1.11917648088113E-18,0.0100000004));
#6872=CARTESIAN_POINT('',(0.03550000008,-0.0374221052,-0.0100000004));
#6873=CARTESIAN_POINT('',(0.03550000008,-0.0746532949430514,-0.0100000004));
#6874=CARTESIAN_POINT('',(0.03650000008,-0.0746532949430514,-0.0100000004));
#6875=CARTESIAN_POINT('',(0.03550000008,-0.0746532949430514,-0.0110000004));
#6876=CARTESIAN_POINT('',(0.03650000008,-0.0582659958948477,-0.0100000004));
#6877=CARTESIAN_POINT('',(0.03550000008,-0.0924221052,-0.0110000004));
#6878=CARTESIAN_POINT('',(0.03650000008,0.,0.));
#6879=CARTESIAN_POINT('',(0.03650000008,-0.0746532949430514,0.));
#6880=CARTESIAN_POINT('',(0.03650000008,-0.0924221052,0.));
#6881=CARTESIAN_POINT('',(0.03650000008,-0.0374221052,0.0110000004));
#6882=CARTESIAN_POINT('',(0.03650000008,-0.0746532949430514,0.0110000004));
#6883=CARTESIAN_POINT('',(0.03650000008,-0.0746532949430514,0.0110000004));
#6884=CARTESIAN_POINT('',(0.03650000008,-0.0374221052,-0.0110000004));
#6885=CARTESIAN_POINT('',(0.03650000008,-0.0746532949430514,-0.0110000004));
#6886=CARTESIAN_POINT('',(0.03650000008,-0.0746532949430514,-0.0110000004));
#6887=CARTESIAN_POINT('',(-0.0196214168703486,-0.0924221052,-0.0669999996));
#6888=CARTESIAN_POINT('',(-0.03100000008,-0.0924221052,0.));
#6889=CARTESIAN_POINT('',(-0.03550000008,-0.0924221052,0.));
#6890=CARTESIAN_POINT('',(-0.03100000008,0.,0.));
#6891=CARTESIAN_POINT('',(-0.03100000008,-0.0746532949430514,0.));
#6892=CARTESIAN_POINT('',(-0.03100000008,-0.0746532949430514,-0.0045));
#6893=CARTESIAN_POINT('',(0.0469715027961281,-0.0924221052,-0.0669999996));
#6894=CARTESIAN_POINT('',(0.03100000008,-0.0924221052,0.));
#6895=CARTESIAN_POINT('',(0.03100000008,-0.0924221052,0.0045));
#6896=CARTESIAN_POINT('',(0.03100000008,0.,0.));
#6897=CARTESIAN_POINT('',(0.03100000008,-0.0746532949430514,0.));
#6898=CARTESIAN_POINT('',(0.03100000008,-0.0746532949430514,-0.0045));
#6899=CARTESIAN_POINT('',(0.0434268042445183,-0.0746532949430514,0.0110000004));
#6900=CARTESIAN_POINT('',(0.0434268042445183,-0.0746532949430514,0.0110000004));
#8534=MECHANICAL_DESIGN_GEOMETRIC_PRESENTATION_REPRESENTATION('',(#4339),#8535);
#8535=(
GEOMETRIC_REPRESENTATION_CONTEXT(3)
GLOBAL_UNCERTAINTY_ASSIGNED_CONTEXT((#8547))
GLOBAL_UNIT_ASSIGNED_CONTEXT((#8561,#8560,#8559))
REPRESENTATION_CONTEXT('MAS-680','TOP_LEVEL_ASSEMBLY_PART')
);
#8541=(
GEOMETRIC_REPRESENTATION_CONTEXT(3)
GLOBAL_UNCERTAINTY_ASSIGNED_CONTEXT((#8553))
GLOBAL_UNIT_ASSIGNED_CONTEXT((#8561,#8560,#8559))
REPRESENTATION_CONTEXT('Part 2','COMPONENT_PART')
);
#8547=UNCERTAINTY_MEASURE_WITH_UNIT(LENGTH_MEASURE(1.E-8),#8561,
'DISTANCE_ACCURACY_VALUE','Maximum Tolerance applied to model');
#8553=UNCERTAINTY_MEASURE_WITH_UNIT(LENGTH_MEASURE(2.E-5),#8561,
'DISTANCE_ACCURACY_VALUE','Maximum Tolerance applied to model');
#8559=(
NAMED_UNIT(*)
SI_UNIT($,.STERADIAN.)
SOLID_ANGLE_UNIT()
);
#8560=(
NAMED_UNIT(*)
PLANE_ANGLE_UNIT()
SI_UNIT($,.RADIAN.)
);
#8561=(
LENGTH_UNIT()
NAMED_UNIT(*)
SI_UNIT($,.METRE.)
);
#8575=PRODUCT_DEFINITION_SHAPE('','',#8595);
#8595=PRODUCT_DEFINITION('','',#8619,#8607);
#8607=PRODUCT_DEFINITION_CONTEXT('',#8674,'design');
#8619=PRODUCT_DEFINITION_FORMATION_WITH_SPECIFIED_SOURCE('','',#8643,
 .NOT_KNOWN.);
#8643=PRODUCT('Part 2','Part 2','Part 2',(#8667));
#8667=PRODUCT_CONTEXT('',#8674,'mechanical');
#8674=APPLICATION_CONTEXT('managed model based 3d engineering');
ENDSEC;
END-ISO-10303-21;
